ISO-10303-21;
HEADER;
/* Generated by software containing ST-Developer
 * from STEP Tools, Inc. (www.steptools.com) 
 */

FILE_DESCRIPTION(
/* description */ ('Self-centering screw clamp'),
/* implementation_level */ '2;1');

FILE_NAME(
/* name */ 'Left screw nut.step',
/* time_stamp */ '2026-10-28T03:25:31-07:00',
/* author */ (''),
/* organization */ (''),
/* preprocessor_version */ 'ST-DEVELOPER v20.2',
/* originating_system */ 'Autodesk Translation Framework v15.17.0.0',
/* authorisation */ '');

FILE_SCHEMA (('AUTOMOTIVE_DESIGN { 1 0 10303 214 3 1 1 }'));
ENDSEC;

DATA;
#10=MECHANICAL_DESIGN_GEOMETRIC_PRESENTATION_REPRESENTATION('',(#653),#16799);
#564=SHAPE_REPRESENTATION_RELATIONSHIP('SRR','None',#17039,#605);
#605=ADVANCED_BREP_SHAPE_REPRESENTATION('',(#701),#16777);
#653=STYLED_ITEM('',(#17333),#701);
#701=MANIFOLD_SOLID_BREP('Body1',#9104);
#899=FACE_BOUND('',#2244,.T.);
#900=FACE_BOUND('',#2247,.T.);
#901=FACE_BOUND('',#2248,.T.);
#902=FACE_BOUND('',#2249,.T.);
#903=FACE_BOUND('',#2252,.T.);
#1146=PLANE('',#10192);
#1147=PLANE('',#10199);
#1148=PLANE('',#10211);
#1149=PLANE('',#10215);
#1150=PLANE('',#10219);
#1553=FACE_OUTER_BOUND('',#2238,.T.);
#1554=FACE_OUTER_BOUND('',#2239,.T.);
#1555=FACE_OUTER_BOUND('',#2240,.T.);
#1556=FACE_OUTER_BOUND('',#2241,.T.);
#1557=FACE_OUTER_BOUND('',#2242,.T.);
#1558=FACE_OUTER_BOUND('',#2243,.T.);
#1559=FACE_OUTER_BOUND('',#2245,.T.);
#1560=FACE_OUTER_BOUND('',#2246,.T.);
#1561=FACE_OUTER_BOUND('',#2250,.T.);
#1562=FACE_OUTER_BOUND('',#2251,.T.);
#2238=EDGE_LOOP('',(#7425,#7426,#7427));
#2239=EDGE_LOOP('',(#7428,#7429,#7430,#7431,#7432,#7433,#7434,#7435));
#2240=EDGE_LOOP('',(#7436,#7437,#7438));
#2241=EDGE_LOOP('',(#7439,#7440,#7441,#7442,#7443,#7444,#7445,#7446));
#2242=EDGE_LOOP('',(#7447,#7448,#7449,#7450,#7451,#7452,#7453,#7454,#7455,
#7456,#7457,#7458));
#2243=EDGE_LOOP('',(#7459));
#2244=EDGE_LOOP('',(#7460,#7461,#7462,#7463,#7464));
#2245=EDGE_LOOP('',(#7465,#7466,#7467,#7468));
#2246=EDGE_LOOP('',(#7469));
#2247=EDGE_LOOP('',(#7470));
#2248=EDGE_LOOP('',(#7471));
#2249=EDGE_LOOP('',(#7472));
#2250=EDGE_LOOP('',(#7473,#7474,#7475,#7476));
#2251=EDGE_LOOP('',(#7477));
#2252=EDGE_LOOP('',(#7478));
#2905=LINE('',#15467,#3478);
#2906=LINE('',#15470,#3479);
#2907=LINE('',#15472,#3480);
#2908=LINE('',#15483,#3481);
#2909=LINE('',#15487,#3482);
#2910=LINE('',#15491,#3483);
#2911=LINE('',#15495,#3484);
#2912=LINE('',#15504,#3485);
#2913=LINE('',#15510,#3486);
#3478=VECTOR('',#12320,1.);
#3479=VECTOR('',#12323,1.);
#3480=VECTOR('',#12324,0.225);
#3481=VECTOR('',#12337,1.);
#3482=VECTOR('',#12340,0.225);
#3483=VECTOR('',#12345,1.);
#3484=VECTOR('',#12350,1.1);
#3485=VECTOR('',#12363,1.6);
#3486=VECTOR('',#12370,0.525);
#4026=CIRCLE('',#10193,1.1);
#4027=CIRCLE('',#10194,0.225);
#4028=CIRCLE('',#10195,0.225);
#4029=CIRCLE('',#10197,0.225);
#4030=CIRCLE('',#10198,0.225);
#4031=CIRCLE('',#10200,1.1);
#4032=CIRCLE('',#10201,0.225);
#4033=CIRCLE('',#10202,1.1);
#4034=CIRCLE('',#10204,0.225);
#4035=CIRCLE('',#10205,0.225);
#4036=CIRCLE('',#10206,0.225);
#4037=CIRCLE('',#10208,1.1);
#4038=CIRCLE('',#10209,1.1);
#4039=CIRCLE('',#10210,1.1);
#4040=CIRCLE('',#10212,1.6);
#4041=CIRCLE('',#10214,1.6);
#4042=CIRCLE('',#10216,0.525);
#4043=CIRCLE('',#10218,0.525);
#4669=VERTEX_POINT('',#15459);
#4670=VERTEX_POINT('',#15460);
#4671=VERTEX_POINT('',#15462);
#4672=VERTEX_POINT('',#15466);
#4673=VERTEX_POINT('',#15468);
#4674=VERTEX_POINT('',#15471);
#4675=VERTEX_POINT('',#15475);
#4676=VERTEX_POINT('',#15476);
#4677=VERTEX_POINT('',#15478);
#4678=VERTEX_POINT('',#15482);
#4679=VERTEX_POINT('',#15484);
#4680=VERTEX_POINT('',#15486);
#4681=VERTEX_POINT('',#15489);
#4682=VERTEX_POINT('',#15494);
#4683=VERTEX_POINT('',#15499);
#4684=VERTEX_POINT('',#15502);
#4685=VERTEX_POINT('',#15506);
#4686=VERTEX_POINT('',#15509);
#5637=EDGE_CURVE('',#4669,#4670,#4026,.T.);
#5638=EDGE_CURVE('',#4669,#4671,#4027,.T.);
#5639=EDGE_CURVE('',#4671,#4670,#4028,.T.);
#5640=EDGE_CURVE('',#4672,#4669,#2905,.T.);
#5641=EDGE_CURVE('',#4673,#4672,#4029,.T.);
#5642=EDGE_CURVE('',#4670,#4673,#2906,.T.);
#5643=EDGE_CURVE('',#4671,#4674,#2907,.T.);
#5644=EDGE_CURVE('',#4674,#4674,#4030,.T.);
#5645=EDGE_CURVE('',#4675,#4676,#4031,.T.);
#5646=EDGE_CURVE('',#4675,#4677,#4032,.T.);
#5647=EDGE_CURVE('',#4676,#4677,#4033,.T.);
#5648=EDGE_CURVE('',#4678,#4675,#2908,.T.);
#5649=EDGE_CURVE('',#4679,#4678,#4034,.T.);
#5650=EDGE_CURVE('',#4679,#4680,#2909,.T.);
#5651=EDGE_CURVE('',#4680,#4680,#4035,.T.);
#5652=EDGE_CURVE('',#4681,#4679,#4036,.T.);
#5653=EDGE_CURVE('',#4677,#4681,#2910,.T.);
#5654=EDGE_CURVE('',#4678,#4673,#4037,.T.);
#5655=EDGE_CURVE('',#4676,#4682,#2911,.T.);
#5656=EDGE_CURVE('',#4682,#4682,#4038,.T.);
#5657=EDGE_CURVE('',#4672,#4681,#4039,.T.);
#5658=EDGE_CURVE('',#4683,#4683,#4040,.T.);
#5659=EDGE_CURVE('',#4684,#4684,#4041,.T.);
#5660=EDGE_CURVE('',#4684,#4683,#2912,.T.);
#5661=EDGE_CURVE('',#4685,#4685,#4042,.T.);
#5662=EDGE_CURVE('',#4685,#4686,#2913,.T.);
#5663=EDGE_CURVE('',#4686,#4686,#4043,.T.);
#7425=ORIENTED_EDGE('',*,*,#5637,.F.);
#7426=ORIENTED_EDGE('',*,*,#5638,.T.);
#7427=ORIENTED_EDGE('',*,*,#5639,.T.);
#7428=ORIENTED_EDGE('',*,*,#5640,.F.);
#7429=ORIENTED_EDGE('',*,*,#5641,.F.);
#7430=ORIENTED_EDGE('',*,*,#5642,.F.);
#7431=ORIENTED_EDGE('',*,*,#5639,.F.);
#7432=ORIENTED_EDGE('',*,*,#5643,.T.);
#7433=ORIENTED_EDGE('',*,*,#5644,.F.);
#7434=ORIENTED_EDGE('',*,*,#5643,.F.);
#7435=ORIENTED_EDGE('',*,*,#5638,.F.);
#7436=ORIENTED_EDGE('',*,*,#5645,.F.);
#7437=ORIENTED_EDGE('',*,*,#5646,.T.);
#7438=ORIENTED_EDGE('',*,*,#5647,.F.);
#7439=ORIENTED_EDGE('',*,*,#5648,.F.);
#7440=ORIENTED_EDGE('',*,*,#5649,.F.);
#7441=ORIENTED_EDGE('',*,*,#5650,.T.);
#7442=ORIENTED_EDGE('',*,*,#5651,.F.);
#7443=ORIENTED_EDGE('',*,*,#5650,.F.);
#7444=ORIENTED_EDGE('',*,*,#5652,.F.);
#7445=ORIENTED_EDGE('',*,*,#5653,.F.);
#7446=ORIENTED_EDGE('',*,*,#5646,.F.);
#7447=ORIENTED_EDGE('',*,*,#5640,.T.);
#7448=ORIENTED_EDGE('',*,*,#5637,.T.);
#7449=ORIENTED_EDGE('',*,*,#5642,.T.);
#7450=ORIENTED_EDGE('',*,*,#5654,.F.);
#7451=ORIENTED_EDGE('',*,*,#5648,.T.);
#7452=ORIENTED_EDGE('',*,*,#5645,.T.);
#7453=ORIENTED_EDGE('',*,*,#5655,.T.);
#7454=ORIENTED_EDGE('',*,*,#5656,.T.);
#7455=ORIENTED_EDGE('',*,*,#5655,.F.);
#7456=ORIENTED_EDGE('',*,*,#5647,.T.);
#7457=ORIENTED_EDGE('',*,*,#5653,.T.);
#7458=ORIENTED_EDGE('',*,*,#5657,.F.);
#7459=ORIENTED_EDGE('',*,*,#5658,.F.);
#7460=ORIENTED_EDGE('',*,*,#5641,.T.);
#7461=ORIENTED_EDGE('',*,*,#5657,.T.);
#7462=ORIENTED_EDGE('',*,*,#5652,.T.);
#7463=ORIENTED_EDGE('',*,*,#5649,.T.);
#7464=ORIENTED_EDGE('',*,*,#5654,.T.);
#7465=ORIENTED_EDGE('',*,*,#5659,.F.);
#7466=ORIENTED_EDGE('',*,*,#5660,.T.);
#7467=ORIENTED_EDGE('',*,*,#5658,.T.);
#7468=ORIENTED_EDGE('',*,*,#5660,.F.);
#7469=ORIENTED_EDGE('',*,*,#5659,.T.);
#7470=ORIENTED_EDGE('',*,*,#5644,.T.);
#7471=ORIENTED_EDGE('',*,*,#5651,.T.);
#7472=ORIENTED_EDGE('',*,*,#5661,.T.);
#7473=ORIENTED_EDGE('',*,*,#5661,.F.);
#7474=ORIENTED_EDGE('',*,*,#5662,.T.);
#7475=ORIENTED_EDGE('',*,*,#5663,.T.);
#7476=ORIENTED_EDGE('',*,*,#5662,.F.);
#7477=ORIENTED_EDGE('',*,*,#5656,.F.);
#7478=ORIENTED_EDGE('',*,*,#5663,.F.);
#8483=CYLINDRICAL_SURFACE('',#10196,0.225);
#8484=CYLINDRICAL_SURFACE('',#10203,0.225);
#8485=CYLINDRICAL_SURFACE('',#10207,1.1);
#8486=CYLINDRICAL_SURFACE('',#10213,1.6);
#8487=CYLINDRICAL_SURFACE('',#10217,0.525);
#8851=ADVANCED_FACE('',(#1553),#1146,.T.);
#8852=ADVANCED_FACE('',(#1554),#8483,.F.);
#8853=ADVANCED_FACE('',(#1555),#1147,.T.);
#8854=ADVANCED_FACE('',(#1556),#8484,.F.);
#8855=ADVANCED_FACE('',(#1557),#8485,.T.);
#8856=ADVANCED_FACE('',(#1558,#899),#1148,.F.);
#8857=ADVANCED_FACE('',(#1559),#8486,.T.);
#8858=ADVANCED_FACE('',(#1560,#900,#901,#902),#1149,.T.);
#8859=ADVANCED_FACE('',(#1561),#8487,.F.);
#8860=ADVANCED_FACE('',(#1562,#903),#1150,.F.);
#9104=CLOSED_SHELL('',(#8851,#8852,#8853,#8854,#8855,#8856,#8857,#8858,
#8859,#8860));
#10191=AXIS2_PLACEMENT_3D('',#15457,#12308,#12309);
#10192=AXIS2_PLACEMENT_3D('',#15458,#12310,#12311);
#10193=AXIS2_PLACEMENT_3D('',#15461,#12312,#12313);
#10194=AXIS2_PLACEMENT_3D('',#15463,#12314,#12315);
#10195=AXIS2_PLACEMENT_3D('',#15464,#12316,#12317);
#10196=AXIS2_PLACEMENT_3D('',#15465,#12318,#12319);
#10197=AXIS2_PLACEMENT_3D('',#15469,#12321,#12322);
#10198=AXIS2_PLACEMENT_3D('',#15473,#12325,#12326);
#10199=AXIS2_PLACEMENT_3D('',#15474,#12327,#12328);
#10200=AXIS2_PLACEMENT_3D('',#15477,#12329,#12330);
#10201=AXIS2_PLACEMENT_3D('',#15479,#12331,#12332);
#10202=AXIS2_PLACEMENT_3D('',#15480,#12333,#12334);
#10203=AXIS2_PLACEMENT_3D('',#15481,#12335,#12336);
#10204=AXIS2_PLACEMENT_3D('',#15485,#12338,#12339);
#10205=AXIS2_PLACEMENT_3D('',#15488,#12341,#12342);
#10206=AXIS2_PLACEMENT_3D('',#15490,#12343,#12344);
#10207=AXIS2_PLACEMENT_3D('',#15492,#12346,#12347);
#10208=AXIS2_PLACEMENT_3D('',#15493,#12348,#12349);
#10209=AXIS2_PLACEMENT_3D('',#15496,#12351,#12352);
#10210=AXIS2_PLACEMENT_3D('',#15497,#12353,#12354);
#10211=AXIS2_PLACEMENT_3D('',#15498,#12355,#12356);
#10212=AXIS2_PLACEMENT_3D('',#15500,#12357,#12358);
#10213=AXIS2_PLACEMENT_3D('',#15501,#12359,#12360);
#10214=AXIS2_PLACEMENT_3D('',#15503,#12361,#12362);
#10215=AXIS2_PLACEMENT_3D('',#15505,#12364,#12365);
#10216=AXIS2_PLACEMENT_3D('',#15507,#12366,#12367);
#10217=AXIS2_PLACEMENT_3D('',#15508,#12368,#12369);
#10218=AXIS2_PLACEMENT_3D('',#15511,#12371,#12372);
#10219=AXIS2_PLACEMENT_3D('',#15512,#12373,#12374);
#12308=DIRECTION('axis',(0.,0.,1.));
#12309=DIRECTION('refdir',(1.,0.,0.));
#12310=DIRECTION('center_axis',(1.,0.,0.));
#12311=DIRECTION('ref_axis',(0.,0.,-1.));
#12312=DIRECTION('center_axis',(-1.,0.,0.));
#12313=DIRECTION('ref_axis',(0.,0.,-1.));
#12314=DIRECTION('center_axis',(1.,0.,0.));
#12315=DIRECTION('ref_axis',(0.,0.,-1.));
#12316=DIRECTION('center_axis',(1.,0.,0.));
#12317=DIRECTION('ref_axis',(0.,0.,-1.));
#12318=DIRECTION('center_axis',(1.,0.,0.));
#12319=DIRECTION('ref_axis',(0.,0.,-1.));
#12320=DIRECTION('',(-1.,0.,0.));
#12321=DIRECTION('center_axis',(1.,0.,0.));
#12322=DIRECTION('ref_axis',(0.,0.,-1.));
#12323=DIRECTION('',(1.,0.,0.));
#12324=DIRECTION('',(1.,0.,0.));
#12325=DIRECTION('center_axis',(-1.,0.,0.));
#12326=DIRECTION('ref_axis',(0.,0.,-1.));
#12327=DIRECTION('center_axis',(1.,0.,0.));
#12328=DIRECTION('ref_axis',(0.,0.,-1.));
#12329=DIRECTION('center_axis',(-1.,0.,0.));
#12330=DIRECTION('ref_axis',(0.,0.,-1.));
#12331=DIRECTION('center_axis',(1.,0.,0.));
#12332=DIRECTION('ref_axis',(0.,0.,-1.));
#12333=DIRECTION('center_axis',(-1.,0.,0.));
#12334=DIRECTION('ref_axis',(0.,0.,-1.));
#12335=DIRECTION('center_axis',(1.,0.,0.));
#12336=DIRECTION('ref_axis',(0.,0.,-1.));
#12337=DIRECTION('',(-1.,0.,0.));
#12338=DIRECTION('center_axis',(1.,0.,0.));
#12339=DIRECTION('ref_axis',(0.,0.,-1.));
#12340=DIRECTION('',(1.,0.,0.));
#12341=DIRECTION('center_axis',(-1.,0.,0.));
#12342=DIRECTION('ref_axis',(0.,0.,-1.));
#12343=DIRECTION('center_axis',(1.,0.,0.));
#12344=DIRECTION('ref_axis',(0.,0.,-1.));
#12345=DIRECTION('',(1.,0.,0.));
#12346=DIRECTION('center_axis',(1.,0.,0.));
#12347=DIRECTION('ref_axis',(0.,0.,-1.));
#12348=DIRECTION('center_axis',(1.,0.,0.));
#12349=DIRECTION('ref_axis',(0.,0.,-1.));
#12350=DIRECTION('',(-1.,0.,0.));
#12351=DIRECTION('center_axis',(1.,0.,0.));
#12352=DIRECTION('ref_axis',(0.,0.,-1.));
#12353=DIRECTION('center_axis',(1.,0.,0.));
#12354=DIRECTION('ref_axis',(0.,0.,-1.));
#12355=DIRECTION('center_axis',(1.,0.,0.));
#12356=DIRECTION('ref_axis',(0.,0.,-1.));
#12357=DIRECTION('center_axis',(1.,0.,0.));
#12358=DIRECTION('ref_axis',(0.,0.,-1.));
#12359=DIRECTION('center_axis',(1.,0.,0.));
#12360=DIRECTION('ref_axis',(0.,0.,-1.));
#12361=DIRECTION('center_axis',(1.,0.,0.));
#12362=DIRECTION('ref_axis',(0.,0.,-1.));
#12363=DIRECTION('',(-1.,0.,0.));
#12364=DIRECTION('center_axis',(1.,0.,0.));
#12365=DIRECTION('ref_axis',(0.,0.,-1.));
#12366=DIRECTION('center_axis',(-1.,0.,0.));
#12367=DIRECTION('ref_axis',(0.,0.,-1.));
#12368=DIRECTION('center_axis',(1.,0.,0.));
#12369=DIRECTION('ref_axis',(0.,0.,-1.));
#12370=DIRECTION('',(-1.,0.,0.));
#12371=DIRECTION('center_axis',(-1.,0.,0.));
#12372=DIRECTION('ref_axis',(0.,0.,-1.));
#12373=DIRECTION('center_axis',(1.,0.,0.));
#12374=DIRECTION('ref_axis',(0.,0.,-1.));
#15457=CARTESIAN_POINT('',(0.,0.,0.));
#15458=CARTESIAN_POINT('Origin',(-5.6,0.,2.7));
#15459=CARTESIAN_POINT('',(-5.6,0.0947295350922144,2.90408653846154));
#15460=CARTESIAN_POINT('',(-5.6,-0.0947295350922144,2.90408653846154));
#15461=CARTESIAN_POINT('Origin',(-5.6,0.,4.));
#15462=CARTESIAN_POINT('',(-5.6,-2.75545529808155E-17,2.925));
#15463=CARTESIAN_POINT('Origin',(-5.6,0.,2.7));
#15464=CARTESIAN_POINT('Origin',(-5.6,0.,2.7));
#15465=CARTESIAN_POINT('Origin',(-5.6,0.,2.7));
#15466=CARTESIAN_POINT('',(-5.5,0.0947295350922147,2.90408653846154));
#15467=CARTESIAN_POINT('',(-5.6,0.0947295350922144,2.90408653846154));
#15468=CARTESIAN_POINT('',(-5.5,-0.0947295350922147,2.90408653846154));
#15469=CARTESIAN_POINT('Origin',(-5.5,0.,2.7));
#15470=CARTESIAN_POINT('',(-5.6,-0.0947295350922144,2.90408653846154));
#15471=CARTESIAN_POINT('',(-5.1,2.75545529808155E-17,2.925));
#15472=CARTESIAN_POINT('',(-5.6,-2.75545529808155E-17,2.925));
#15473=CARTESIAN_POINT('Origin',(-5.1,0.,2.7));
#15474=CARTESIAN_POINT('Origin',(-5.6,0.,5.3));
#15475=CARTESIAN_POINT('',(-5.6,-0.0947295350922135,5.09591346153846));
#15476=CARTESIAN_POINT('',(-5.6,-1.34711147906209E-16,5.1));
#15477=CARTESIAN_POINT('Origin',(-5.6,0.,4.));
#15478=CARTESIAN_POINT('',(-5.6,0.0947295350922135,5.09591346153846));
#15479=CARTESIAN_POINT('Origin',(-5.6,0.,5.3));
#15480=CARTESIAN_POINT('Origin',(-5.6,0.,4.));
#15481=CARTESIAN_POINT('Origin',(-5.6,0.,5.3));
#15482=CARTESIAN_POINT('',(-5.5,-0.0947295350922147,5.09591346153846));
#15483=CARTESIAN_POINT('',(-5.6,-0.0947295350922135,5.09591346153846));
#15484=CARTESIAN_POINT('',(-5.5,-2.75545529808154E-17,5.525));
#15485=CARTESIAN_POINT('Origin',(-5.5,0.,5.3));
#15486=CARTESIAN_POINT('',(-5.1,2.75545529808154E-17,5.525));
#15487=CARTESIAN_POINT('',(-5.6,-2.75545529808154E-17,5.525));
#15488=CARTESIAN_POINT('Origin',(-5.1,0.,5.3));
#15489=CARTESIAN_POINT('',(-5.5,0.0947295350922147,5.09591346153846));
#15490=CARTESIAN_POINT('Origin',(-5.5,0.,5.3));
#15491=CARTESIAN_POINT('',(-5.6,0.0947295350922135,5.09591346153846));
#15492=CARTESIAN_POINT('Origin',(-8.5,0.,4.));
#15493=CARTESIAN_POINT('Origin',(-5.5,0.,4.));
#15494=CARTESIAN_POINT('',(-8.5,-1.34711147906209E-16,5.1));
#15495=CARTESIAN_POINT('',(-8.5,-1.34711147906209E-16,5.1));
#15496=CARTESIAN_POINT('Origin',(-8.5,0.,4.));
#15497=CARTESIAN_POINT('Origin',(-5.5,0.,4.));
#15498=CARTESIAN_POINT('Origin',(-5.5,0.,4.));
#15499=CARTESIAN_POINT('',(-5.5,-1.95943487863577E-16,5.6));
#15500=CARTESIAN_POINT('Origin',(-5.5,0.,4.));
#15501=CARTESIAN_POINT('Origin',(-5.5,0.,4.));
#15502=CARTESIAN_POINT('',(-5.1,-1.95943487863577E-16,5.6));
#15503=CARTESIAN_POINT('Origin',(-5.1,0.,4.));
#15504=CARTESIAN_POINT('',(-5.5,-1.95943487863577E-16,5.6));
#15505=CARTESIAN_POINT('Origin',(-5.1,0.,4.));
#15506=CARTESIAN_POINT('',(-5.1,-6.4293956955236E-17,4.525));
#15507=CARTESIAN_POINT('Origin',(-5.1,0.,4.));
#15508=CARTESIAN_POINT('Origin',(-8.5,0.,4.));
#15509=CARTESIAN_POINT('',(-8.5,-6.4293956955236E-17,4.525));
#15510=CARTESIAN_POINT('',(-8.5,-6.4293956955236E-17,4.525));
#15511=CARTESIAN_POINT('Origin',(-8.5,0.,4.));
#15512=CARTESIAN_POINT('Origin',(-8.5,0.,4.));
#16728=UNCERTAINTY_MEASURE_WITH_UNIT(LENGTH_MEASURE(0.001),#16800,
'DISTANCE_ACCURACY_VALUE',
'Maximum model space distance between geometric entities at asserted c
onnectivities');
#16750=UNCERTAINTY_MEASURE_WITH_UNIT(LENGTH_MEASURE(0.001),#16800,
'DISTANCE_ACCURACY_VALUE',
'Maximum model space distance between geometric entities at asserted c
onnectivities');
#16777=(
GEOMETRIC_REPRESENTATION_CONTEXT(3)
GLOBAL_UNCERTAINTY_ASSIGNED_CONTEXT((#16728))
GLOBAL_UNIT_ASSIGNED_CONTEXT((#16800,#16802,#16803))
REPRESENTATION_CONTEXT('','3D')
);
#16799=(
GEOMETRIC_REPRESENTATION_CONTEXT(3)
GLOBAL_UNCERTAINTY_ASSIGNED_CONTEXT((#16750))
GLOBAL_UNIT_ASSIGNED_CONTEXT((#16800,#16802,#16803))
REPRESENTATION_CONTEXT('','3D')
);
#16800=(
LENGTH_UNIT()
NAMED_UNIT(*)
SI_UNIT(.CENTI.,.METRE.)
);
#16802=(
NAMED_UNIT(*)
PLANE_ANGLE_UNIT()
SI_UNIT($,.RADIAN.)
);
#16803=(
NAMED_UNIT(*)
SI_UNIT($,.STERADIAN.)
SOLID_ANGLE_UNIT()
);
#16830=SHAPE_DEFINITION_REPRESENTATION(#16883,#17039);
#16883=PRODUCT_DEFINITION_SHAPE('',$,#17088);
#17039=SHAPE_REPRESENTATION('',(#10191),#16777);
#17061=PRODUCT_DEFINITION_CONTEXT('part definition',#17207,'design');
#17088=PRODUCT_DEFINITION('Left screw nut','Left screw nut',#17136,#17061);
#17136=PRODUCT_DEFINITION_FORMATION('',$,#17235);
#17207=APPLICATION_CONTEXT(
'Core Data for Automotive Mechanical Design Process');
#17208=PRODUCT_CONTEXT('part definition',#17207,'mechanical');
#17235=PRODUCT('Left screw nut','Left screw nut','Left screw nut',(#17208));
#17327=COLOUR_RGB('Black',0.12,0.14,0.17);
#17328=FILL_AREA_STYLE_COLOUR('',#17327);
#17329=FILL_AREA_STYLE('',(#17328));
#17330=SURFACE_STYLE_FILL_AREA(#17329);
#17331=SURFACE_SIDE_STYLE('',(#17330));
#17332=SURFACE_STYLE_USAGE(.BOTH.,#17331);
#17333=PRESENTATION_STYLE_ASSIGNMENT((#17332));
ENDSEC;
END-ISO-10303-21;
